ISO-10303-21;
HEADER;
/* Generated by software containing ST-Developer
 * from STEP Tools, Inc. (www.steptools.com) 
 */

FILE_DESCRIPTION(
/* description */ ('Independent two-stage semi-open centrifugal-pump CAD. Shared impeller
s, open-machinable return casings, removable diaphragms, bronze wear/j
ournal rings, volume-preserving seal instances, retained keyed shaft, 
opposed mechanical face rings and partly threaded tie hardware. Native
 shaft rotation. Geometric topology/clearance only; flow/head/efficien
cy, pressure, cavitation, balance, preload, face loading and secondary
 seal fits/bonds, material/thermal/tolerance selection and life unassi
gned. External drive, coupling, anchors and piping bolts omitted.'),
/* implementation_level */ '2;1');

FILE_NAME(
/* name */ 'Shaft thrust washer.step',
/* time_stamp */ '2026-11-08T18:06:32-08:00',
/* author */ (''),
/* organization */ (''),
/* preprocessor_version */ 'ST-DEVELOPER v20.2',
/* originating_system */ 'Autodesk Translation Framework v15.17.0.0',
/* authorisation */ '');

FILE_SCHEMA (('AUTOMOTIVE_DESIGN { 1 0 10303 214 3 1 1 }'));
ENDSEC;

DATA;
#10=MECHANICAL_DESIGN_GEOMETRIC_PRESENTATION_REPRESENTATION('',(#409),#16687);
#371=SHAPE_REPRESENTATION_RELATIONSHIP('SRR','None',#16780,#390);
#390=ADVANCED_BREP_SHAPE_REPRESENTATION('',(#428),#16684);
#409=STYLED_ITEM('',(#16879),#428);
#428=MANIFOLD_SOLID_BREP('Body1',#6128);
#549=FACE_BOUND('',#1460,.T.);
#550=FACE_BOUND('',#1462,.T.);
#669=PLANE('',#6905);
#670=PLANE('',#6906);
#992=FACE_OUTER_BOUND('',#1457,.T.);
#993=FACE_OUTER_BOUND('',#1458,.T.);
#994=FACE_OUTER_BOUND('',#1459,.T.);
#995=FACE_OUTER_BOUND('',#1461,.T.);
#1457=EDGE_LOOP('',(#5365,#5366,#5367,#5368));
#1458=EDGE_LOOP('',(#5369,#5370,#5371,#5372));
#1459=EDGE_LOOP('',(#5373));
#1460=EDGE_LOOP('',(#5374));
#1461=EDGE_LOOP('',(#5375));
#1462=EDGE_LOOP('',(#5376));
#1826=LINE('',#15237,#2195);
#1827=LINE('',#15243,#2196);
#2195=VECTOR('',#8432,1.);
#2196=VECTOR('',#8439,1.4);
#2482=CIRCLE('',#6900,1.);
#2483=CIRCLE('',#6901,1.);
#2484=CIRCLE('',#6903,1.4);
#2485=CIRCLE('',#6904,1.4);
#2989=VERTEX_POINT('',#15234);
#2990=VERTEX_POINT('',#15236);
#2991=VERTEX_POINT('',#15240);
#2992=VERTEX_POINT('',#15242);
#3792=EDGE_CURVE('',#2989,#2989,#2482,.T.);
#3793=EDGE_CURVE('',#2989,#2990,#1826,.T.);
#3794=EDGE_CURVE('',#2990,#2990,#2483,.T.);
#3795=EDGE_CURVE('',#2991,#2991,#2484,.T.);
#3796=EDGE_CURVE('',#2991,#2992,#1827,.T.);
#3797=EDGE_CURVE('',#2992,#2992,#2485,.T.);
#5365=ORIENTED_EDGE('',*,*,#3792,.F.);
#5366=ORIENTED_EDGE('',*,*,#3793,.T.);
#5367=ORIENTED_EDGE('',*,*,#3794,.T.);
#5368=ORIENTED_EDGE('',*,*,#3793,.F.);
#5369=ORIENTED_EDGE('',*,*,#3795,.F.);
#5370=ORIENTED_EDGE('',*,*,#3796,.T.);
#5371=ORIENTED_EDGE('',*,*,#3797,.T.);
#5372=ORIENTED_EDGE('',*,*,#3796,.F.);
#5373=ORIENTED_EDGE('',*,*,#3795,.T.);
#5374=ORIENTED_EDGE('',*,*,#3792,.T.);
#5375=ORIENTED_EDGE('',*,*,#3797,.F.);
#5376=ORIENTED_EDGE('',*,*,#3794,.F.);
#5744=CYLINDRICAL_SURFACE('',#6899,1.);
#5745=CYLINDRICAL_SURFACE('',#6902,1.4);
#6071=ADVANCED_FACE('',(#992),#5744,.F.);
#6072=ADVANCED_FACE('',(#993),#5745,.T.);
#6073=ADVANCED_FACE('',(#994,#549),#669,.T.);
#6074=ADVANCED_FACE('',(#995,#550),#670,.F.);
#6128=CLOSED_SHELL('',(#6071,#6072,#6073,#6074));
#6898=AXIS2_PLACEMENT_3D('',#15232,#8426,#8427);
#6899=AXIS2_PLACEMENT_3D('',#15233,#8428,#8429);
#6900=AXIS2_PLACEMENT_3D('',#15235,#8430,#8431);
#6901=AXIS2_PLACEMENT_3D('',#15238,#8433,#8434);
#6902=AXIS2_PLACEMENT_3D('',#15239,#8435,#8436);
#6903=AXIS2_PLACEMENT_3D('',#15241,#8437,#8438);
#6904=AXIS2_PLACEMENT_3D('',#15244,#8440,#8441);
#6905=AXIS2_PLACEMENT_3D('',#15245,#8442,#8443);
#6906=AXIS2_PLACEMENT_3D('',#15246,#8444,#8445);
#8426=DIRECTION('axis',(0.,0.,1.));
#8427=DIRECTION('refdir',(1.,0.,0.));
#8428=DIRECTION('center_axis',(0.,0.,1.));
#8429=DIRECTION('ref_axis',(1.,0.,0.));
#8430=DIRECTION('center_axis',(0.,0.,-1.));
#8431=DIRECTION('ref_axis',(1.,0.,0.));
#8432=DIRECTION('',(0.,0.,-1.));
#8433=DIRECTION('center_axis',(0.,0.,-1.));
#8434=DIRECTION('ref_axis',(1.,0.,0.));
#8435=DIRECTION('center_axis',(0.,0.,1.));
#8436=DIRECTION('ref_axis',(1.,0.,0.));
#8437=DIRECTION('center_axis',(0.,0.,1.));
#8438=DIRECTION('ref_axis',(1.,0.,0.));
#8439=DIRECTION('',(0.,0.,-1.));
#8440=DIRECTION('center_axis',(0.,0.,1.));
#8441=DIRECTION('ref_axis',(1.,0.,0.));
#8442=DIRECTION('center_axis',(0.,0.,1.));
#8443=DIRECTION('ref_axis',(1.,0.,0.));
#8444=DIRECTION('center_axis',(0.,0.,1.));
#8445=DIRECTION('ref_axis',(1.,0.,0.));
#15232=CARTESIAN_POINT('',(0.,0.,0.));
#15233=CARTESIAN_POINT('Origin',(0.,0.,0.));
#15234=CARTESIAN_POINT('',(-1.,-1.22464679914735E-16,0.2));
#15235=CARTESIAN_POINT('Origin',(0.,0.,0.2));
#15236=CARTESIAN_POINT('',(-1.,-1.22464679914735E-16,0.));
#15237=CARTESIAN_POINT('',(-1.,-1.22464679914735E-16,0.));
#15238=CARTESIAN_POINT('Origin',(0.,0.,0.));
#15239=CARTESIAN_POINT('Origin',(0.,0.,0.));
#15240=CARTESIAN_POINT('',(-1.4,-1.71450551880629E-16,0.2));
#15241=CARTESIAN_POINT('Origin',(0.,0.,0.2));
#15242=CARTESIAN_POINT('',(-1.4,-1.71450551880629E-16,0.));
#15243=CARTESIAN_POINT('',(-1.4,-1.71450551880629E-16,0.));
#15244=CARTESIAN_POINT('Origin',(0.,0.,0.));
#15245=CARTESIAN_POINT('Origin',(0.,0.,0.2));
#15246=CARTESIAN_POINT('Origin',(0.,0.,0.));
#16663=UNCERTAINTY_MEASURE_WITH_UNIT(LENGTH_MEASURE(0.001),#16688,
'DISTANCE_ACCURACY_VALUE',
'Maximum model space distance between geometric entities at asserted c
onnectivities');
#16666=UNCERTAINTY_MEASURE_WITH_UNIT(LENGTH_MEASURE(0.001),#16688,
'DISTANCE_ACCURACY_VALUE',
'Maximum model space distance between geometric entities at asserted c
onnectivities');
#16684=(
GEOMETRIC_REPRESENTATION_CONTEXT(3)
GLOBAL_UNCERTAINTY_ASSIGNED_CONTEXT((#16663))
GLOBAL_UNIT_ASSIGNED_CONTEXT((#16688,#16690,#16691))
REPRESENTATION_CONTEXT('','3D')
);
#16687=(
GEOMETRIC_REPRESENTATION_CONTEXT(3)
GLOBAL_UNCERTAINTY_ASSIGNED_CONTEXT((#16666))
GLOBAL_UNIT_ASSIGNED_CONTEXT((#16688,#16690,#16691))
REPRESENTATION_CONTEXT('','3D')
);
#16688=(
LENGTH_UNIT()
NAMED_UNIT(*)
SI_UNIT(.CENTI.,.METRE.)
);
#16690=(
NAMED_UNIT(*)
PLANE_ANGLE_UNIT()
SI_UNIT($,.RADIAN.)
);
#16691=(
NAMED_UNIT(*)
SI_UNIT($,.STERADIAN.)
SOLID_ANGLE_UNIT()
);
#16709=SHAPE_DEFINITION_REPRESENTATION(#16729,#16780);
#16729=PRODUCT_DEFINITION_SHAPE('',$,#16801);
#16780=SHAPE_REPRESENTATION('',(#6898),#16684);
#16783=PRODUCT_DEFINITION_CONTEXT('part definition',#16845,'design');
#16801=PRODUCT_DEFINITION('Shaft thrust washer','Shaft thrust washer',#16821,
#16783);
#16821=PRODUCT_DEFINITION_FORMATION('',$,#16864);
#16845=APPLICATION_CONTEXT(
'Core Data for Automotive Mechanical Design Process');
#16846=PRODUCT_CONTEXT('part definition',#16845,'mechanical');
#16864=PRODUCT('Shaft thrust washer','Shaft thrust washer',$,(#16846));
#16879=PRESENTATION_STYLE_ASSIGNMENT((#16894));
#16894=SURFACE_STYLE_USAGE(.BOTH.,#16909);
#16909=SURFACE_SIDE_STYLE('',(#16924));
#16924=SURFACE_STYLE_FILL_AREA(#16939);
#16939=FILL_AREA_STYLE('Washer gray',(#16954));
#16954=FILL_AREA_STYLE_COLOUR('Washer gray',#16969);
#16969=COLOUR_RGB('Washer gray',0.725490196078431,0.752941176470588,0.792156862745098);
ENDSEC;
END-ISO-10303-21;
